ISO-10303-21;
HEADER;
/* Generated by software containing ST-Developer
 * from STEP Tools, Inc. (www.steptools.com) 
 */

FILE_DESCRIPTION(
/* description */ ('PAT-001'),
/* implementation_level */ '2;1');

FILE_NAME(
/* name */ 'Cap Screw - M4x16.step',
/* time_stamp */ '2026-10-29T17:07:15-07:00',
/* author */ (''),
/* organization */ (''),
/* preprocessor_version */ 'ST-DEVELOPER v20.2',
/* originating_system */ 'Autodesk Translation Framework v15.17.0.0',
/* authorisation */ '');

FILE_SCHEMA (('AUTOMOTIVE_DESIGN { 1 0 10303 214 3 1 1 }'));
ENDSEC;

DATA;
#10=MECHANICAL_DESIGN_GEOMETRIC_PRESENTATION_REPRESENTATION('',(#405),#9622);
#30=ORIENTED_CLOSED_SHELL('',*,#5232,.F.);
#32=BREP_WITH_VOIDS('Body1',#5231,(#30));
#317=CONICAL_SURFACE('',#6030,0.325,0.785398163397448);
#318=CONICAL_SURFACE('',#6034,0.335,0.785398163397448);
#319=CONICAL_SURFACE('',#6038,0.21,0.463647609000806);
#320=CONICAL_SURFACE('',#6042,0.18,0.785398163397448);
#347=SHAPE_REPRESENTATION_RELATIONSHIP('SRR','None',#9772,#372);
#372=ADVANCED_BREP_SHAPE_REPRESENTATION('',(#32),#9621);
#405=STYLED_ITEM('',(#9969),#32);
#527=FACE_BOUND('',#1385,.T.);
#704=PLANE('',#6028);
#705=PLANE('',#6036);
#706=PLANE('',#6044);
#707=PLANE('',#6045);
#708=PLANE('',#6046);
#709=PLANE('',#6047);
#710=PLANE('',#6048);
#711=PLANE('',#6049);
#712=PLANE('',#6050);
#713=PLANE('',#6051);
#714=PLANE('',#6052);
#994=FACE_OUTER_BOUND('',#1380,.T.);
#995=FACE_OUTER_BOUND('',#1381,.T.);
#996=FACE_OUTER_BOUND('',#1382,.T.);
#997=FACE_OUTER_BOUND('',#1383,.T.);
#998=FACE_OUTER_BOUND('',#1384,.T.);
#999=FACE_OUTER_BOUND('',#1386,.T.);
#1000=FACE_OUTER_BOUND('',#1387,.T.);
#1001=FACE_OUTER_BOUND('',#1388,.T.);
#1002=FACE_OUTER_BOUND('',#1389,.T.);
#1003=FACE_OUTER_BOUND('',#1390,.T.);
#1004=FACE_OUTER_BOUND('',#1391,.T.);
#1005=FACE_OUTER_BOUND('',#1392,.T.);
#1006=FACE_OUTER_BOUND('',#1393,.T.);
#1007=FACE_OUTER_BOUND('',#1394,.T.);
#1008=FACE_OUTER_BOUND('',#1395,.T.);
#1009=FACE_OUTER_BOUND('',#1396,.T.);
#1010=FACE_OUTER_BOUND('',#1397,.T.);
#1380=EDGE_LOOP('',(#4763));
#1381=EDGE_LOOP('',(#4764,#4765,#4766,#4767));
#1382=EDGE_LOOP('',(#4768,#4769,#4770,#4771));
#1383=EDGE_LOOP('',(#4772,#4773,#4774,#4775));
#1384=EDGE_LOOP('',(#4776));
#1385=EDGE_LOOP('',(#4777));
#1386=EDGE_LOOP('',(#4778,#4779,#4780,#4781));
#1387=EDGE_LOOP('',(#4782,#4783,#4784,#4785));
#1388=EDGE_LOOP('',(#4786,#4787,#4788,#4789));
#1389=EDGE_LOOP('',(#4790));
#1390=EDGE_LOOP('',(#4791,#4792,#4793,#4794));
#1391=EDGE_LOOP('',(#4795,#4796,#4797,#4798));
#1392=EDGE_LOOP('',(#4799,#4800,#4801,#4802));
#1393=EDGE_LOOP('',(#4803,#4804,#4805,#4806));
#1394=EDGE_LOOP('',(#4807,#4808,#4809,#4810));
#1395=EDGE_LOOP('',(#4811,#4812,#4813,#4814));
#1396=EDGE_LOOP('',(#4815,#4816,#4817,#4818,#4819,#4820));
#1397=EDGE_LOOP('',(#4821,#4822,#4823,#4824,#4825,#4826));
#1779=LINE('',#9446,#2184);
#1780=LINE('',#9450,#2185);
#1781=LINE('',#9454,#2186);
#1782=LINE('',#9461,#2187);
#1783=LINE('',#9465,#2188);
#1784=LINE('',#9469,#2189);
#1785=LINE('',#9474,#2190);
#1786=LINE('',#9476,#2191);
#1787=LINE('',#9478,#2192);
#1788=LINE('',#9479,#2193);
#1789=LINE('',#9482,#2194);
#1790=LINE('',#9484,#2195);
#1791=LINE('',#9485,#2196);
#1792=LINE('',#9488,#2197);
#1793=LINE('',#9490,#2198);
#1794=LINE('',#9491,#2199);
#1795=LINE('',#9494,#2200);
#1796=LINE('',#9496,#2201);
#1797=LINE('',#9497,#2202);
#1798=LINE('',#9500,#2203);
#1799=LINE('',#9502,#2204);
#1800=LINE('',#9503,#2205);
#1801=LINE('',#9505,#2206);
#1802=LINE('',#9506,#2207);
#2184=VECTOR('',#7534,0.325);
#2185=VECTOR('',#7539,0.35);
#2186=VECTOR('',#7544,0.335);
#2187=VECTOR('',#7553,0.21);
#2188=VECTOR('',#7558,0.2);
#2189=VECTOR('',#7563,0.18);
#2190=VECTOR('',#7568,1.);
#2191=VECTOR('',#7569,1.);
#2192=VECTOR('',#7570,1.);
#2193=VECTOR('',#7571,1.);
#2194=VECTOR('',#7574,1.);
#2195=VECTOR('',#7575,1.);
#2196=VECTOR('',#7576,1.);
#2197=VECTOR('',#7579,1.);
#2198=VECTOR('',#7580,1.);
#2199=VECTOR('',#7581,1.);
#2200=VECTOR('',#7584,1.);
#2201=VECTOR('',#7585,1.);
#2202=VECTOR('',#7586,1.);
#2203=VECTOR('',#7589,1.);
#2204=VECTOR('',#7590,1.);
#2205=VECTOR('',#7591,1.);
#2206=VECTOR('',#7594,1.);
#2207=VECTOR('',#7595,1.);
#2412=CIRCLE('',#6029,0.3);
#2413=CIRCLE('',#6031,0.35);
#2414=CIRCLE('',#6033,0.35);
#2415=CIRCLE('',#6035,0.32);
#2416=CIRCLE('',#6037,0.22);
#2417=CIRCLE('',#6039,0.1954);
#2418=CIRCLE('',#6041,0.1954);
#2419=CIRCLE('',#6043,0.16);
#2842=VERTEX_POINT('',#9441);
#2843=VERTEX_POINT('',#9444);
#2844=VERTEX_POINT('',#9448);
#2845=VERTEX_POINT('',#9452);
#2846=VERTEX_POINT('',#9456);
#2847=VERTEX_POINT('',#9459);
#2848=VERTEX_POINT('',#9463);
#2849=VERTEX_POINT('',#9467);
#2850=VERTEX_POINT('',#9472);
#2851=VERTEX_POINT('',#9473);
#2852=VERTEX_POINT('',#9475);
#2853=VERTEX_POINT('',#9477);
#2854=VERTEX_POINT('',#9481);
#2855=VERTEX_POINT('',#9483);
#2856=VERTEX_POINT('',#9487);
#2857=VERTEX_POINT('',#9489);
#2858=VERTEX_POINT('',#9493);
#2859=VERTEX_POINT('',#9495);
#2860=VERTEX_POINT('',#9499);
#2861=VERTEX_POINT('',#9501);
#3485=EDGE_CURVE('',#2842,#2842,#2412,.T.);
#3486=EDGE_CURVE('',#2843,#2843,#2413,.T.);
#3487=EDGE_CURVE('',#2843,#2842,#1779,.T.);
#3488=EDGE_CURVE('',#2844,#2844,#2414,.T.);
#3489=EDGE_CURVE('',#2844,#2843,#1780,.T.);
#3490=EDGE_CURVE('',#2845,#2845,#2415,.T.);
#3491=EDGE_CURVE('',#2845,#2844,#1781,.T.);
#3492=EDGE_CURVE('',#2846,#2846,#2416,.T.);
#3493=EDGE_CURVE('',#2847,#2847,#2417,.F.);
#3494=EDGE_CURVE('',#2847,#2846,#1782,.T.);
#3495=EDGE_CURVE('',#2848,#2848,#2418,.F.);
#3496=EDGE_CURVE('',#2848,#2847,#1783,.T.);
#3497=EDGE_CURVE('',#2849,#2849,#2419,.T.);
#3498=EDGE_CURVE('',#2849,#2848,#1784,.T.);
#3499=EDGE_CURVE('',#2850,#2851,#1785,.T.);
#3500=EDGE_CURVE('',#2851,#2852,#1786,.T.);
#3501=EDGE_CURVE('',#2852,#2853,#1787,.T.);
#3502=EDGE_CURVE('',#2850,#2853,#1788,.T.);
#3503=EDGE_CURVE('',#2851,#2854,#1789,.T.);
#3504=EDGE_CURVE('',#2854,#2855,#1790,.T.);
#3505=EDGE_CURVE('',#2855,#2852,#1791,.T.);
#3506=EDGE_CURVE('',#2854,#2856,#1792,.T.);
#3507=EDGE_CURVE('',#2856,#2857,#1793,.T.);
#3508=EDGE_CURVE('',#2857,#2855,#1794,.T.);
#3509=EDGE_CURVE('',#2856,#2858,#1795,.T.);
#3510=EDGE_CURVE('',#2858,#2859,#1796,.T.);
#3511=EDGE_CURVE('',#2859,#2857,#1797,.T.);
#3512=EDGE_CURVE('',#2858,#2860,#1798,.T.);
#3513=EDGE_CURVE('',#2860,#2861,#1799,.T.);
#3514=EDGE_CURVE('',#2861,#2859,#1800,.T.);
#3515=EDGE_CURVE('',#2860,#2850,#1801,.T.);
#3516=EDGE_CURVE('',#2853,#2861,#1802,.T.);
#4763=ORIENTED_EDGE('',*,*,#3485,.F.);
#4764=ORIENTED_EDGE('',*,*,#3486,.F.);
#4765=ORIENTED_EDGE('',*,*,#3487,.T.);
#4766=ORIENTED_EDGE('',*,*,#3485,.T.);
#4767=ORIENTED_EDGE('',*,*,#3487,.F.);
#4768=ORIENTED_EDGE('',*,*,#3488,.F.);
#4769=ORIENTED_EDGE('',*,*,#3489,.T.);
#4770=ORIENTED_EDGE('',*,*,#3486,.T.);
#4771=ORIENTED_EDGE('',*,*,#3489,.F.);
#4772=ORIENTED_EDGE('',*,*,#3490,.F.);
#4773=ORIENTED_EDGE('',*,*,#3491,.T.);
#4774=ORIENTED_EDGE('',*,*,#3488,.T.);
#4775=ORIENTED_EDGE('',*,*,#3491,.F.);
#4776=ORIENTED_EDGE('',*,*,#3490,.T.);
#4777=ORIENTED_EDGE('',*,*,#3492,.F.);
#4778=ORIENTED_EDGE('',*,*,#3493,.F.);
#4779=ORIENTED_EDGE('',*,*,#3494,.T.);
#4780=ORIENTED_EDGE('',*,*,#3492,.T.);
#4781=ORIENTED_EDGE('',*,*,#3494,.F.);
#4782=ORIENTED_EDGE('',*,*,#3495,.F.);
#4783=ORIENTED_EDGE('',*,*,#3496,.T.);
#4784=ORIENTED_EDGE('',*,*,#3493,.T.);
#4785=ORIENTED_EDGE('',*,*,#3496,.F.);
#4786=ORIENTED_EDGE('',*,*,#3497,.F.);
#4787=ORIENTED_EDGE('',*,*,#3498,.T.);
#4788=ORIENTED_EDGE('',*,*,#3495,.T.);
#4789=ORIENTED_EDGE('',*,*,#3498,.F.);
#4790=ORIENTED_EDGE('',*,*,#3497,.T.);
#4791=ORIENTED_EDGE('',*,*,#3499,.T.);
#4792=ORIENTED_EDGE('',*,*,#3500,.T.);
#4793=ORIENTED_EDGE('',*,*,#3501,.T.);
#4794=ORIENTED_EDGE('',*,*,#3502,.F.);
#4795=ORIENTED_EDGE('',*,*,#3503,.T.);
#4796=ORIENTED_EDGE('',*,*,#3504,.T.);
#4797=ORIENTED_EDGE('',*,*,#3505,.T.);
#4798=ORIENTED_EDGE('',*,*,#3500,.F.);
#4799=ORIENTED_EDGE('',*,*,#3506,.T.);
#4800=ORIENTED_EDGE('',*,*,#3507,.T.);
#4801=ORIENTED_EDGE('',*,*,#3508,.T.);
#4802=ORIENTED_EDGE('',*,*,#3504,.F.);
#4803=ORIENTED_EDGE('',*,*,#3509,.T.);
#4804=ORIENTED_EDGE('',*,*,#3510,.T.);
#4805=ORIENTED_EDGE('',*,*,#3511,.T.);
#4806=ORIENTED_EDGE('',*,*,#3507,.F.);
#4807=ORIENTED_EDGE('',*,*,#3512,.T.);
#4808=ORIENTED_EDGE('',*,*,#3513,.T.);
#4809=ORIENTED_EDGE('',*,*,#3514,.T.);
#4810=ORIENTED_EDGE('',*,*,#3510,.F.);
#4811=ORIENTED_EDGE('',*,*,#3515,.T.);
#4812=ORIENTED_EDGE('',*,*,#3502,.T.);
#4813=ORIENTED_EDGE('',*,*,#3516,.T.);
#4814=ORIENTED_EDGE('',*,*,#3513,.F.);
#4815=ORIENTED_EDGE('',*,*,#3515,.F.);
#4816=ORIENTED_EDGE('',*,*,#3512,.F.);
#4817=ORIENTED_EDGE('',*,*,#3509,.F.);
#4818=ORIENTED_EDGE('',*,*,#3506,.F.);
#4819=ORIENTED_EDGE('',*,*,#3503,.F.);
#4820=ORIENTED_EDGE('',*,*,#3499,.F.);
#4821=ORIENTED_EDGE('',*,*,#3516,.F.);
#4822=ORIENTED_EDGE('',*,*,#3501,.F.);
#4823=ORIENTED_EDGE('',*,*,#3505,.F.);
#4824=ORIENTED_EDGE('',*,*,#3508,.F.);
#4825=ORIENTED_EDGE('',*,*,#3511,.F.);
#4826=ORIENTED_EDGE('',*,*,#3514,.F.);
#4900=CYLINDRICAL_SURFACE('',#6032,0.35);
#4901=CYLINDRICAL_SURFACE('',#6040,0.1954);
#5181=ADVANCED_FACE('',(#994),#704,.T.);
#5182=ADVANCED_FACE('',(#995),#317,.T.);
#5183=ADVANCED_FACE('',(#996),#4900,.T.);
#5184=ADVANCED_FACE('',(#997),#318,.T.);
#5185=ADVANCED_FACE('',(#998,#527),#705,.T.);
#5186=ADVANCED_FACE('',(#999),#319,.T.);
#5187=ADVANCED_FACE('',(#1000),#4901,.T.);
#5188=ADVANCED_FACE('',(#1001),#320,.T.);
#5189=ADVANCED_FACE('',(#1002),#706,.T.);
#5190=ADVANCED_FACE('',(#1003),#707,.F.);
#5191=ADVANCED_FACE('',(#1004),#708,.F.);
#5192=ADVANCED_FACE('',(#1005),#709,.F.);
#5193=ADVANCED_FACE('',(#1006),#710,.F.);
#5194=ADVANCED_FACE('',(#1007),#711,.F.);
#5195=ADVANCED_FACE('',(#1008),#712,.F.);
#5196=ADVANCED_FACE('',(#1009),#713,.F.);
#5197=ADVANCED_FACE('',(#1010),#714,.F.);
#5231=CLOSED_SHELL('',(#5181,#5182,#5183,#5184,#5185,#5186,#5187,#5188,
#5189));
#5232=CLOSED_SHELL('',(#5190,#5191,#5192,#5193,#5194,#5195,#5196,#5197));
#6027=AXIS2_PLACEMENT_3D('',#9439,#7524,#7525);
#6028=AXIS2_PLACEMENT_3D('',#9440,#7526,#7527);
#6029=AXIS2_PLACEMENT_3D('',#9442,#7528,#7529);
#6030=AXIS2_PLACEMENT_3D('',#9443,#7530,#7531);
#6031=AXIS2_PLACEMENT_3D('',#9445,#7532,#7533);
#6032=AXIS2_PLACEMENT_3D('',#9447,#7535,#7536);
#6033=AXIS2_PLACEMENT_3D('',#9449,#7537,#7538);
#6034=AXIS2_PLACEMENT_3D('',#9451,#7540,#7541);
#6035=AXIS2_PLACEMENT_3D('',#9453,#7542,#7543);
#6036=AXIS2_PLACEMENT_3D('',#9455,#7545,#7546);
#6037=AXIS2_PLACEMENT_3D('',#9457,#7547,#7548);
#6038=AXIS2_PLACEMENT_3D('',#9458,#7549,#7550);
#6039=AXIS2_PLACEMENT_3D('',#9460,#7551,#7552);
#6040=AXIS2_PLACEMENT_3D('',#9462,#7554,#7555);
#6041=AXIS2_PLACEMENT_3D('',#9464,#7556,#7557);
#6042=AXIS2_PLACEMENT_3D('',#9466,#7559,#7560);
#6043=AXIS2_PLACEMENT_3D('',#9468,#7561,#7562);
#6044=AXIS2_PLACEMENT_3D('',#9470,#7564,#7565);
#6045=AXIS2_PLACEMENT_3D('',#9471,#7566,#7567);
#6046=AXIS2_PLACEMENT_3D('',#9480,#7572,#7573);
#6047=AXIS2_PLACEMENT_3D('',#9486,#7577,#7578);
#6048=AXIS2_PLACEMENT_3D('',#9492,#7582,#7583);
#6049=AXIS2_PLACEMENT_3D('',#9498,#7587,#7588);
#6050=AXIS2_PLACEMENT_3D('',#9504,#7592,#7593);
#6051=AXIS2_PLACEMENT_3D('',#9507,#7596,#7597);
#6052=AXIS2_PLACEMENT_3D('',#9508,#7598,#7599);
#7524=DIRECTION('axis',(0.,0.,1.));
#7525=DIRECTION('refdir',(1.,0.,0.));
#7526=DIRECTION('center_axis',(0.,1.,0.));
#7527=DIRECTION('ref_axis',(0.,0.,1.));
#7528=DIRECTION('center_axis',(0.,-1.,0.));
#7529=DIRECTION('ref_axis',(1.,0.,0.));
#7530=DIRECTION('center_axis',(0.,-1.,0.));
#7531=DIRECTION('ref_axis',(1.,0.,0.));
#7532=DIRECTION('center_axis',(0.,-1.,0.));
#7533=DIRECTION('ref_axis',(1.,0.,0.));
#7534=DIRECTION('',(0.707106781186547,0.707106781186548,8.65956056235493E-17));
#7535=DIRECTION('center_axis',(0.,-1.,0.));
#7536=DIRECTION('ref_axis',(1.,0.,0.));
#7537=DIRECTION('center_axis',(0.,-1.,0.));
#7538=DIRECTION('ref_axis',(1.,0.,0.));
#7539=DIRECTION('',(0.,1.,0.));
#7540=DIRECTION('center_axis',(0.,1.,0.));
#7541=DIRECTION('ref_axis',(1.,0.,0.));
#7542=DIRECTION('center_axis',(0.,-1.,0.));
#7543=DIRECTION('ref_axis',(1.,0.,0.));
#7544=DIRECTION('',(-0.707106781186547,0.707106781186548,-8.65956056235493E-17));
#7545=DIRECTION('center_axis',(0.,-1.,0.));
#7546=DIRECTION('ref_axis',(0.,0.,-1.));
#7547=DIRECTION('center_axis',(0.,-1.,0.));
#7548=DIRECTION('ref_axis',(1.,0.,0.));
#7549=DIRECTION('center_axis',(0.,1.,0.));
#7550=DIRECTION('ref_axis',(1.,0.,0.));
#7551=DIRECTION('center_axis',(0.,1.,0.));
#7552=DIRECTION('ref_axis',(1.,0.,0.));
#7553=DIRECTION('',(-0.447213595499958,0.894427190999916,-5.47678698264203E-17));
#7554=DIRECTION('center_axis',(0.,-1.,0.));
#7555=DIRECTION('ref_axis',(1.,0.,0.));
#7556=DIRECTION('center_axis',(0.,1.,0.));
#7557=DIRECTION('ref_axis',(1.,0.,0.));
#7558=DIRECTION('',(0.,1.,0.));
#7559=DIRECTION('center_axis',(0.,1.,0.));
#7560=DIRECTION('ref_axis',(1.,0.,0.));
#7561=DIRECTION('center_axis',(0.,-1.,0.));
#7562=DIRECTION('ref_axis',(1.,0.,0.));
#7563=DIRECTION('',(-0.707106781186547,0.707106781186548,-8.65956056235493E-17));
#7564=DIRECTION('center_axis',(0.,-1.,0.));
#7565=DIRECTION('ref_axis',(0.,0.,-1.));
#7566=DIRECTION('center_axis',(0.866025403784439,0.,-0.5));
#7567=DIRECTION('ref_axis',(0.5,0.,0.866025403784439));
#7568=DIRECTION('',(-0.5,0.,-0.866025403784439));
#7569=DIRECTION('',(0.,-1.,0.));
#7570=DIRECTION('',(0.5,0.,0.866025403784439));
#7571=DIRECTION('',(0.,-1.,0.));
#7572=DIRECTION('center_axis',(1.60246890531964E-16,0.,-1.));
#7573=DIRECTION('ref_axis',(1.,0.,1.60246890531964E-16));
#7574=DIRECTION('',(-1.,0.,-1.60246890531964E-16));
#7575=DIRECTION('',(0.,-1.,0.));
#7576=DIRECTION('',(1.,0.,1.60246890531964E-16));
#7577=DIRECTION('center_axis',(-0.866025403784439,0.,-0.5));
#7578=DIRECTION('ref_axis',(0.5,0.,-0.866025403784439));
#7579=DIRECTION('',(-0.5,0.,0.866025403784439));
#7580=DIRECTION('',(0.,-1.,0.));
#7581=DIRECTION('',(0.5,0.,-0.866025403784439));
#7582=DIRECTION('center_axis',(-0.866025403784439,0.,0.5));
#7583=DIRECTION('ref_axis',(-0.5,0.,-0.866025403784439));
#7584=DIRECTION('',(0.5,0.,0.866025403784439));
#7585=DIRECTION('',(0.,-1.,0.));
#7586=DIRECTION('',(-0.5,0.,-0.866025403784439));
#7587=DIRECTION('center_axis',(-1.60246890531964E-16,0.,1.));
#7588=DIRECTION('ref_axis',(-1.,0.,-1.60246890531964E-16));
#7589=DIRECTION('',(1.,0.,1.60246890531964E-16));
#7590=DIRECTION('',(0.,-1.,0.));
#7591=DIRECTION('',(-1.,0.,-1.60246890531964E-16));
#7592=DIRECTION('center_axis',(0.866025403784439,0.,0.5));
#7593=DIRECTION('ref_axis',(-0.5,0.,0.866025403784439));
#7594=DIRECTION('',(0.5,0.,-0.866025403784439));
#7595=DIRECTION('',(-0.5,0.,0.866025403784439));
#7596=DIRECTION('center_axis',(0.,1.,0.));
#7597=DIRECTION('ref_axis',(1.,0.,0.));
#7598=DIRECTION('center_axis',(0.,-1.,0.));
#7599=DIRECTION('ref_axis',(0.,0.,-1.));
#9439=CARTESIAN_POINT('',(0.,0.,0.));
#9440=CARTESIAN_POINT('Origin',(0.3,0.4,0.));
#9441=CARTESIAN_POINT('',(-0.3,0.4,-3.67394039744206E-17));
#9442=CARTESIAN_POINT('Origin',(0.,0.4,0.));
#9443=CARTESIAN_POINT('Origin',(0.,0.375,0.));
#9444=CARTESIAN_POINT('',(-0.35,0.35,-4.28626379701573E-17));
#9445=CARTESIAN_POINT('Origin',(0.,0.35,0.));
#9446=CARTESIAN_POINT('',(-0.325,0.375,-3.9801020972289E-17));
#9447=CARTESIAN_POINT('Origin',(0.,0.19,0.));
#9448=CARTESIAN_POINT('',(-0.35,0.03,-4.28626379701574E-17));
#9449=CARTESIAN_POINT('Origin',(0.,0.03,0.));
#9450=CARTESIAN_POINT('',(-0.35,0.19,-4.28626379701574E-17));
#9451=CARTESIAN_POINT('Origin',(0.,0.0149999999999999,0.));
#9452=CARTESIAN_POINT('',(-0.32,-3.29597460435593E-17,-3.91886975727153E-17));
#9453=CARTESIAN_POINT('Origin',(0.,0.,0.));
#9454=CARTESIAN_POINT('',(-0.335,0.0149999999999999,-4.10256677714363E-17));
#9455=CARTESIAN_POINT('Origin',(0.22,0.,0.));
#9456=CARTESIAN_POINT('',(-0.22,-6.93889390390723E-18,-2.69422295812418E-17));
#9457=CARTESIAN_POINT('Origin',(0.,0.,0.));
#9458=CARTESIAN_POINT('Origin',(0.,-0.02,0.));
#9459=CARTESIAN_POINT('',(-0.1954,-0.0492,2.39295984553393E-17));
#9460=CARTESIAN_POINT('Origin',(0.,-0.0492,0.));
#9461=CARTESIAN_POINT('',(-0.21,-0.02,-2.57175827820944E-17));
#9462=CARTESIAN_POINT('Origin',(0.,-0.8,0.));
#9463=CARTESIAN_POINT('',(-0.1954,-1.5646,2.39295984553393E-17));
#9464=CARTESIAN_POINT('Origin',(0.,-1.5646,0.));
#9465=CARTESIAN_POINT('',(-0.1954,-0.8,-2.39295984553393E-17));
#9466=CARTESIAN_POINT('Origin',(0.,-1.58,0.));
#9467=CARTESIAN_POINT('',(-0.16,-1.6,-1.95943487863577E-17));
#9468=CARTESIAN_POINT('Origin',(0.,-1.6,0.));
#9469=CARTESIAN_POINT('',(-0.18,-1.58,-2.20436423846524E-17));
#9470=CARTESIAN_POINT('Origin',(0.,-1.6,0.));
#9471=CARTESIAN_POINT('Origin',(0.0866025403784439,-0.4,-0.15));
#9472=CARTESIAN_POINT('',(0.173205080756888,-0.4,0.));
#9473=CARTESIAN_POINT('',(0.0866025403784439,-0.4,-0.15));
#9474=CARTESIAN_POINT('',(0.173205080756888,-0.4,0.));
#9475=CARTESIAN_POINT('',(0.0866025403784439,-0.64,-0.15));
#9476=CARTESIAN_POINT('',(0.0866025403784439,-0.4,-0.15));
#9477=CARTESIAN_POINT('',(0.173205080756888,-0.64,0.));
#9478=CARTESIAN_POINT('',(0.173205080756888,-0.64,0.));
#9479=CARTESIAN_POINT('',(0.173205080756888,-0.4,0.));
#9480=CARTESIAN_POINT('Origin',(-0.0866025403784438,-0.4,-0.15));
#9481=CARTESIAN_POINT('',(-0.0866025403784438,-0.4,-0.15));
#9482=CARTESIAN_POINT('',(0.0866025403784439,-0.4,-0.15));
#9483=CARTESIAN_POINT('',(-0.0866025403784438,-0.64,-0.15));
#9484=CARTESIAN_POINT('',(-0.0866025403784438,-0.4,-0.15));
#9485=CARTESIAN_POINT('',(0.0866025403784439,-0.64,-0.15));
#9486=CARTESIAN_POINT('Origin',(-0.173205080756888,-0.4,-2.77555756156289E-17));
#9487=CARTESIAN_POINT('',(-0.173205080756888,-0.4,-2.12115047744981E-17));
#9488=CARTESIAN_POINT('',(-0.0866025403784438,-0.4,-0.15));
#9489=CARTESIAN_POINT('',(-0.173205080756888,-0.64,-2.77555756156289E-17));
#9490=CARTESIAN_POINT('',(-0.173205080756888,-0.4,-2.12115047744981E-17));
#9491=CARTESIAN_POINT('',(-0.0866025403784438,-0.64,-0.15));
#9492=CARTESIAN_POINT('Origin',(-0.0866025403784439,-0.4,0.15));
#9493=CARTESIAN_POINT('',(-0.0866025403784439,-0.4,0.15));
#9494=CARTESIAN_POINT('',(-0.173205080756888,-0.4,-2.12115047744981E-17));
#9495=CARTESIAN_POINT('',(-0.0866025403784439,-0.64,0.15));
#9496=CARTESIAN_POINT('',(-0.0866025403784439,-0.4,0.15));
#9497=CARTESIAN_POINT('',(-0.173205080756888,-0.64,-2.12115047744981E-17));
#9498=CARTESIAN_POINT('Origin',(0.0866025403784439,-0.4,0.15));
#9499=CARTESIAN_POINT('',(0.0866025403784439,-0.4,0.15));
#9500=CARTESIAN_POINT('',(-0.0866025403784439,-0.4,0.15));
#9501=CARTESIAN_POINT('',(0.0866025403784439,-0.64,0.15));
#9502=CARTESIAN_POINT('',(0.0866025403784439,-0.4,0.15));
#9503=CARTESIAN_POINT('',(-0.0866025403784439,-0.64,0.15));
#9504=CARTESIAN_POINT('Origin',(0.173205080756888,-0.4,0.));
#9505=CARTESIAN_POINT('',(0.0866025403784439,-0.4,0.15));
#9506=CARTESIAN_POINT('',(0.0866025403784439,-0.64,0.15));
#9507=CARTESIAN_POINT('Origin',(0.,-0.4,-2.77555756156289E-17));
#9508=CARTESIAN_POINT('Origin',(0.,-0.64,-2.77555756156289E-17));
#9591=UNCERTAINTY_MEASURE_WITH_UNIT(LENGTH_MEASURE(0.001),#9623,
'DISTANCE_ACCURACY_VALUE',
'Maximum model space distance between geometric entities at asserted c
onnectivities');
#9592=UNCERTAINTY_MEASURE_WITH_UNIT(LENGTH_MEASURE(0.001),#9623,
'DISTANCE_ACCURACY_VALUE',
'Maximum model space distance between geometric entities at asserted c
onnectivities');
#9621=(
GEOMETRIC_REPRESENTATION_CONTEXT(3)
GLOBAL_UNCERTAINTY_ASSIGNED_CONTEXT((#9591))
GLOBAL_UNIT_ASSIGNED_CONTEXT((#9623,#9625,#9626))
REPRESENTATION_CONTEXT('','3D')
);
#9622=(
GEOMETRIC_REPRESENTATION_CONTEXT(3)
GLOBAL_UNCERTAINTY_ASSIGNED_CONTEXT((#9592))
GLOBAL_UNIT_ASSIGNED_CONTEXT((#9623,#9625,#9626))
REPRESENTATION_CONTEXT('','3D')
);
#9623=(
LENGTH_UNIT()
NAMED_UNIT(*)
SI_UNIT(.CENTI.,.METRE.)
);
#9625=(
NAMED_UNIT(*)
PLANE_ANGLE_UNIT()
SI_UNIT($,.RADIAN.)
);
#9626=(
NAMED_UNIT(*)
SI_UNIT($,.STERADIAN.)
SOLID_ANGLE_UNIT()
);
#9655=SHAPE_DEFINITION_REPRESENTATION(#9689,#9772);
#9689=PRODUCT_DEFINITION_SHAPE('',$,#9802);
#9772=SHAPE_REPRESENTATION('',(#6027),#9621);
#9773=PRODUCT_DEFINITION_CONTEXT('part definition',#9862,'design');
#9802=PRODUCT_DEFINITION('Cap Screw - M4x16','Cap Screw - M4x16',#9831,
#9773);
#9831=PRODUCT_DEFINITION_FORMATION('',$,#9892);
#9862=APPLICATION_CONTEXT(
'Core Data for Automotive Mechanical Design Process');
#9863=PRODUCT_CONTEXT('part definition',#9862,'mechanical');
#9892=PRODUCT('Cap Screw - M4x16','Cap Screw - M4x16',
'Cap Screw - M4x16',(#9863));
#9963=COLOUR_RGB('Black',0.12,0.14,0.17);
#9964=FILL_AREA_STYLE_COLOUR('',#9963);
#9965=FILL_AREA_STYLE('',(#9964));
#9966=SURFACE_STYLE_FILL_AREA(#9965);
#9967=SURFACE_SIDE_STYLE('',(#9966));
#9968=SURFACE_STYLE_USAGE(.BOTH.,#9967);
#9969=PRESENTATION_STYLE_ASSIGNMENT((#9968));
ENDSEC;
END-ISO-10303-21;
